ISO-10303-21;
HEADER;
/* Generated by software containing ST-Developer
 * from STEP Tools, Inc. (www.steptools.com) 
 */

FILE_DESCRIPTION(
/* description */ ('Belt conveyor head drive unit'),
/* implementation_level */ '2;1');

FILE_NAME(
/* name */ 'Output M3 set screw (1).step',
/* time_stamp */ '2026-10-28T03:26:19-07:00',
/* author */ (''),
/* organization */ (''),
/* preprocessor_version */ 'ST-DEVELOPER v20.2',
/* originating_system */ 'Autodesk Translation Framework v15.17.0.0',
/* authorisation */ '');

FILE_SCHEMA (('AUTOMOTIVE_DESIGN { 1 0 10303 214 3 1 1 }'));
ENDSEC;

DATA;
#10=MECHANICAL_DESIGN_GEOMETRIC_PRESENTATION_REPRESENTATION('',(#920),#27069);
#766=SHAPE_REPRESENTATION_RELATIONSHIP('SRR','None',#27415,#835);
#835=ADVANCED_BREP_SHAPE_REPRESENTATION('',(#1001),#27057);
#920=STYLED_ITEM('',(#27804),#1001);
#1001=MANIFOLD_SOLID_BREP('Body1',#13789);
#1582=PLANE('',#15918);
#1583=PLANE('',#15919);
#2264=FACE_OUTER_BOUND('',#3292,.T.);
#2265=FACE_OUTER_BOUND('',#3293,.T.);
#2266=FACE_OUTER_BOUND('',#3294,.T.);
#3292=EDGE_LOOP('',(#11676,#11677,#11678,#11679));
#3293=EDGE_LOOP('',(#11680));
#3294=EDGE_LOOP('',(#11681));
#4126=LINE('',#25393,#4918);
#4918=VECTOR('',#19772,0.15);
#5727=CIRCLE('',#15916,0.15);
#5728=CIRCLE('',#15917,0.15);
#6883=VERTEX_POINT('',#25390);
#6884=VERTEX_POINT('',#25392);
#8530=EDGE_CURVE('',#6883,#6883,#5727,.T.);
#8531=EDGE_CURVE('',#6883,#6884,#4126,.T.);
#8532=EDGE_CURVE('',#6884,#6884,#5728,.T.);
#11676=ORIENTED_EDGE('',*,*,#8530,.F.);
#11677=ORIENTED_EDGE('',*,*,#8531,.T.);
#11678=ORIENTED_EDGE('',*,*,#8532,.T.);
#11679=ORIENTED_EDGE('',*,*,#8531,.F.);
#11680=ORIENTED_EDGE('',*,*,#8530,.T.);
#11681=ORIENTED_EDGE('',*,*,#8532,.F.);
#12800=CYLINDRICAL_SURFACE('',#15915,0.15);
#13543=ADVANCED_FACE('',(#2264),#12800,.T.);
#13544=ADVANCED_FACE('',(#2265),#1582,.T.);
#13545=ADVANCED_FACE('',(#2266),#1583,.F.);
#13789=CLOSED_SHELL('',(#13543,#13544,#13545));
#15914=AXIS2_PLACEMENT_3D('',#25388,#19766,#19767);
#15915=AXIS2_PLACEMENT_3D('',#25389,#19768,#19769);
#15916=AXIS2_PLACEMENT_3D('',#25391,#19770,#19771);
#15917=AXIS2_PLACEMENT_3D('',#25394,#19773,#19774);
#15918=AXIS2_PLACEMENT_3D('',#25395,#19775,#19776);
#15919=AXIS2_PLACEMENT_3D('',#25396,#19777,#19778);
#19766=DIRECTION('axis',(0.,0.,1.));
#19767=DIRECTION('refdir',(1.,0.,0.));
#19768=DIRECTION('center_axis',(0.,0.,1.));
#19769=DIRECTION('ref_axis',(1.,0.,0.));
#19770=DIRECTION('center_axis',(0.,0.,1.));
#19771=DIRECTION('ref_axis',(1.,0.,0.));
#19772=DIRECTION('',(0.,0.,-1.));
#19773=DIRECTION('center_axis',(0.,0.,1.));
#19774=DIRECTION('ref_axis',(1.,0.,0.));
#19775=DIRECTION('center_axis',(0.,0.,1.));
#19776=DIRECTION('ref_axis',(1.,0.,0.));
#19777=DIRECTION('center_axis',(0.,0.,1.));
#19778=DIRECTION('ref_axis',(1.,0.,0.));
#25388=CARTESIAN_POINT('',(0.,0.,0.));
#25389=CARTESIAN_POINT('Origin',(6.97091003018116,-4.,7.6));
#25390=CARTESIAN_POINT('',(6.82091003018116,-4.,8.));
#25391=CARTESIAN_POINT('Origin',(6.97091003018116,-4.,8.));
#25392=CARTESIAN_POINT('',(6.82091003018116,-4.,7.6));
#25393=CARTESIAN_POINT('',(6.82091003018116,-4.,7.6));
#25394=CARTESIAN_POINT('Origin',(6.97091003018116,-4.,7.6));
#25395=CARTESIAN_POINT('Origin',(6.97091003018116,-4.,8.));
#25396=CARTESIAN_POINT('Origin',(6.97091003018116,-4.,7.6));
#26980=UNCERTAINTY_MEASURE_WITH_UNIT(LENGTH_MEASURE(0.001),#27070,
'DISTANCE_ACCURACY_VALUE',
'Maximum model space distance between geometric entities at asserted c
onnectivities');
#26992=UNCERTAINTY_MEASURE_WITH_UNIT(LENGTH_MEASURE(0.001),#27070,
'DISTANCE_ACCURACY_VALUE',
'Maximum model space distance between geometric entities at asserted c
onnectivities');
#27057=(
GEOMETRIC_REPRESENTATION_CONTEXT(3)
GLOBAL_UNCERTAINTY_ASSIGNED_CONTEXT((#26980))
GLOBAL_UNIT_ASSIGNED_CONTEXT((#27070,#27072,#27073))
REPRESENTATION_CONTEXT('','3D')
);
#27069=(
GEOMETRIC_REPRESENTATION_CONTEXT(3)
GLOBAL_UNCERTAINTY_ASSIGNED_CONTEXT((#26992))
GLOBAL_UNIT_ASSIGNED_CONTEXT((#27070,#27072,#27073))
REPRESENTATION_CONTEXT('','3D')
);
#27070=(
LENGTH_UNIT()
NAMED_UNIT(*)
SI_UNIT(.CENTI.,.METRE.)
);
#27072=(
NAMED_UNIT(*)
PLANE_ANGLE_UNIT()
SI_UNIT($,.RADIAN.)
);
#27073=(
NAMED_UNIT(*)
SI_UNIT($,.STERADIAN.)
SOLID_ANGLE_UNIT()
);
#27138=SHAPE_DEFINITION_REPRESENTATION(#27226,#27415);
#27226=PRODUCT_DEFINITION_SHAPE('',$,#27492);
#27415=SHAPE_REPRESENTATION('',(#15914),#27057);
#27427=PRODUCT_DEFINITION_CONTEXT('part definition',#27657,'design');
#27492=PRODUCT_DEFINITION('Output M3 set screw (1)',
'Output M3 set screw (1)',#27568,#27427);
#27568=PRODUCT_DEFINITION_FORMATION('',$,#27723);
#27657=APPLICATION_CONTEXT(
'Core Data for Automotive Mechanical Design Process');
#27658=PRODUCT_CONTEXT('part definition',#27657,'mechanical');
#27723=PRODUCT('Output M3 set screw (1)','Output M3 set screw (1)',
'Output M3 set screw (1)',(#27658));
#27798=COLOUR_RGB('Black',0.12,0.14,0.17);
#27799=FILL_AREA_STYLE_COLOUR('',#27798);
#27800=FILL_AREA_STYLE('',(#27799));
#27801=SURFACE_STYLE_FILL_AREA(#27800);
#27802=SURFACE_SIDE_STYLE('',(#27801));
#27803=SURFACE_STYLE_USAGE(.BOTH.,#27802);
#27804=PRESENTATION_STYLE_ASSIGNMENT((#27803));
ENDSEC;
END-ISO-10303-21;
